ISO-10303-21;
HEADER;
/* Generated by software containing ST-Developer
 * from STEP Tools, Inc. (www.steptools.com) 
 */

FILE_DESCRIPTION(
/* description */ ('Cam-and-follower valve demonstrator'),
/* implementation_level */ '2;1');

FILE_NAME(
/* name */ 'Inner race sleeve 15 mm (1).step',
/* time_stamp */ '2026-10-28T03:25:17-07:00',
/* author */ (''),
/* organization */ (''),
/* preprocessor_version */ 'ST-DEVELOPER v20.2',
/* originating_system */ 'Autodesk Translation Framework v15.17.0.0',
/* authorisation */ '');

FILE_SCHEMA (('AUTOMOTIVE_DESIGN { 1 0 10303 214 3 1 1 }'));
ENDSEC;

DATA;
#10=MECHANICAL_DESIGN_GEOMETRIC_PRESENTATION_REPRESENTATION('',(#444),#12896);
#365=SHAPE_REPRESENTATION_RELATIONSHIP('SRR','None',#13084,#401);
#401=ADVANCED_BREP_SHAPE_REPRESENTATION('',(#485),#12884);
#444=STYLED_ITEM('',(#13330),#485);
#485=MANIFOLD_SOLID_BREP('Body1',#6213);
#636=FACE_BOUND('',#1889,.T.);
#637=FACE_BOUND('',#1891,.T.);
#919=CIRCLE('',#7202,0.605);
#920=CIRCLE('',#7203,0.605);
#921=CIRCLE('',#7205,0.8);
#922=CIRCLE('',#7206,0.8);
#1071=CYLINDRICAL_SURFACE('',#7201,0.605);
#1072=CYLINDRICAL_SURFACE('',#7204,0.8);
#1377=FACE_OUTER_BOUND('',#1886,.T.);
#1378=FACE_OUTER_BOUND('',#1887,.T.);
#1379=FACE_OUTER_BOUND('',#1888,.T.);
#1380=FACE_OUTER_BOUND('',#1890,.T.);
#1886=EDGE_LOOP('',(#5275,#5276,#5277,#5278));
#1887=EDGE_LOOP('',(#5279,#5280,#5281,#5282));
#1888=EDGE_LOOP('',(#5283));
#1889=EDGE_LOOP('',(#5284));
#1890=EDGE_LOOP('',(#5285));
#1891=EDGE_LOOP('',(#5286));
#2310=LINE('',#12389,#2732);
#2311=LINE('',#12395,#2733);
#2732=VECTOR('',#8891,0.605);
#2733=VECTOR('',#8898,0.8);
#3238=VERTEX_POINT('',#12386);
#3239=VERTEX_POINT('',#12388);
#3240=VERTEX_POINT('',#12392);
#3241=VERTEX_POINT('',#12394);
#3934=EDGE_CURVE('',#3238,#3238,#919,.T.);
#3935=EDGE_CURVE('',#3238,#3239,#2310,.T.);
#3936=EDGE_CURVE('',#3239,#3239,#920,.T.);
#3937=EDGE_CURVE('',#3240,#3240,#921,.T.);
#3938=EDGE_CURVE('',#3240,#3241,#2311,.T.);
#3939=EDGE_CURVE('',#3241,#3241,#922,.T.);
#5275=ORIENTED_EDGE('',*,*,#3934,.F.);
#5276=ORIENTED_EDGE('',*,*,#3935,.T.);
#5277=ORIENTED_EDGE('',*,*,#3936,.T.);
#5278=ORIENTED_EDGE('',*,*,#3935,.F.);
#5279=ORIENTED_EDGE('',*,*,#3937,.F.);
#5280=ORIENTED_EDGE('',*,*,#3938,.T.);
#5281=ORIENTED_EDGE('',*,*,#3939,.T.);
#5282=ORIENTED_EDGE('',*,*,#3938,.F.);
#5283=ORIENTED_EDGE('',*,*,#3937,.T.);
#5284=ORIENTED_EDGE('',*,*,#3934,.T.);
#5285=ORIENTED_EDGE('',*,*,#3939,.F.);
#5286=ORIENTED_EDGE('',*,*,#3936,.F.);
#5753=PLANE('',#7207);
#5754=PLANE('',#7208);
#6093=ADVANCED_FACE('',(#1377),#1071,.F.);
#6094=ADVANCED_FACE('',(#1378),#1072,.T.);
#6095=ADVANCED_FACE('',(#1379,#636),#5753,.T.);
#6096=ADVANCED_FACE('',(#1380,#637),#5754,.F.);
#6213=CLOSED_SHELL('',(#6093,#6094,#6095,#6096));
#7200=AXIS2_PLACEMENT_3D('',#12384,#8885,#8886);
#7201=AXIS2_PLACEMENT_3D('',#12385,#8887,#8888);
#7202=AXIS2_PLACEMENT_3D('',#12387,#8889,#8890);
#7203=AXIS2_PLACEMENT_3D('',#12390,#8892,#8893);
#7204=AXIS2_PLACEMENT_3D('',#12391,#8894,#8895);
#7205=AXIS2_PLACEMENT_3D('',#12393,#8896,#8897);
#7206=AXIS2_PLACEMENT_3D('',#12396,#8899,#8900);
#7207=AXIS2_PLACEMENT_3D('',#12397,#8901,#8902);
#7208=AXIS2_PLACEMENT_3D('',#12398,#8903,#8904);
#8885=DIRECTION('axis',(0.,0.,1.));
#8886=DIRECTION('refdir',(1.,0.,0.));
#8887=DIRECTION('center_axis',(0.,1.,0.));
#8888=DIRECTION('ref_axis',(1.,0.,0.));
#8889=DIRECTION('center_axis',(0.,-1.,0.));
#8890=DIRECTION('ref_axis',(1.,0.,0.));
#8891=DIRECTION('',(0.,-1.,0.));
#8892=DIRECTION('center_axis',(0.,-1.,0.));
#8893=DIRECTION('ref_axis',(1.,0.,0.));
#8894=DIRECTION('center_axis',(0.,1.,0.));
#8895=DIRECTION('ref_axis',(1.,0.,0.));
#8896=DIRECTION('center_axis',(0.,1.,0.));
#8897=DIRECTION('ref_axis',(1.,0.,0.));
#8898=DIRECTION('',(0.,-1.,0.));
#8899=DIRECTION('center_axis',(0.,1.,0.));
#8900=DIRECTION('ref_axis',(1.,0.,0.));
#8901=DIRECTION('center_axis',(0.,1.,0.));
#8902=DIRECTION('ref_axis',(1.,0.,0.));
#8903=DIRECTION('center_axis',(0.,1.,0.));
#8904=DIRECTION('ref_axis',(1.,0.,0.));
#12384=CARTESIAN_POINT('',(0.,0.,0.));
#12385=CARTESIAN_POINT('Origin',(0.,3.,4.));
#12386=CARTESIAN_POINT('',(-0.605,4.5,4.));
#12387=CARTESIAN_POINT('Origin',(0.,4.5,4.));
#12388=CARTESIAN_POINT('',(-0.605,3.,4.));
#12389=CARTESIAN_POINT('',(-0.605,3.,4.));
#12390=CARTESIAN_POINT('Origin',(0.,3.,4.));
#12391=CARTESIAN_POINT('Origin',(0.,3.,4.));
#12392=CARTESIAN_POINT('',(-0.8,4.5,4.));
#12393=CARTESIAN_POINT('Origin',(0.,4.5,4.));
#12394=CARTESIAN_POINT('',(-0.8,3.,4.));
#12395=CARTESIAN_POINT('',(-0.8,3.,4.));
#12396=CARTESIAN_POINT('Origin',(0.,3.,4.));
#12397=CARTESIAN_POINT('Origin',(0.,4.5,4.));
#12398=CARTESIAN_POINT('Origin',(0.,3.,4.));
#12841=UNCERTAINTY_MEASURE_WITH_UNIT(LENGTH_MEASURE(0.001),#12897,
'DISTANCE_ACCURACY_VALUE',
'Maximum model space distance between geometric entities at asserted c
onnectivities');
#12853=UNCERTAINTY_MEASURE_WITH_UNIT(LENGTH_MEASURE(0.001),#12897,
'DISTANCE_ACCURACY_VALUE',
'Maximum model space distance between geometric entities at asserted c
onnectivities');
#12884=(
GEOMETRIC_REPRESENTATION_CONTEXT(3)
GLOBAL_UNCERTAINTY_ASSIGNED_CONTEXT((#12841))
GLOBAL_UNIT_ASSIGNED_CONTEXT((#12897,#12899,#12900))
REPRESENTATION_CONTEXT('','3D')
);
#12896=(
GEOMETRIC_REPRESENTATION_CONTEXT(3)
GLOBAL_UNCERTAINTY_ASSIGNED_CONTEXT((#12853))
GLOBAL_UNIT_ASSIGNED_CONTEXT((#12897,#12899,#12900))
REPRESENTATION_CONTEXT('','3D')
);
#12897=(
LENGTH_UNIT()
NAMED_UNIT(*)
SI_UNIT(.CENTI.,.METRE.)
);
#12899=(
NAMED_UNIT(*)
PLANE_ANGLE_UNIT()
SI_UNIT($,.RADIAN.)
);
#12900=(
NAMED_UNIT(*)
SI_UNIT($,.STERADIAN.)
SOLID_ANGLE_UNIT()
);
#12931=SHAPE_DEFINITION_REPRESENTATION(#12980,#13084);
#12980=PRODUCT_DEFINITION_SHAPE('',$,#13127);
#13084=SHAPE_REPRESENTATION('',(#7200),#12884);
#13096=PRODUCT_DEFINITION_CONTEXT('part definition',#13224,'design');
#13127=PRODUCT_DEFINITION('Inner race sleeve 15 mm (1)',
'Inner race sleeve 15 mm (1)',#13169,#13096);
#13169=PRODUCT_DEFINITION_FORMATION('',$,#13256);
#13224=APPLICATION_CONTEXT(
'Core Data for Automotive Mechanical Design Process');
#13225=PRODUCT_CONTEXT('part definition',#13224,'mechanical');
#13256=PRODUCT('Inner race sleeve 15 mm (1)',
'Inner race sleeve 15 mm (1)','Inner race sleeve 15 mm (1)',(#13225));
#13324=COLOUR_RGB('Grey',0.48,0.52,0.57);
#13325=FILL_AREA_STYLE_COLOUR('',#13324);
#13326=FILL_AREA_STYLE('',(#13325));
#13327=SURFACE_STYLE_FILL_AREA(#13326);
#13328=SURFACE_SIDE_STYLE('',(#13327));
#13329=SURFACE_STYLE_USAGE(.BOTH.,#13328);
#13330=PRESENTATION_STYLE_ASSIGNMENT((#13329));
ENDSEC;
END-ISO-10303-21;
